ISO-10303-21;
HEADER;
FILE_DESCRIPTION (('STEP AP214'),
    '1' );
FILE_NAME ('Rod base.step',
    '2026-10-07T06:38:26',
    ( '' ),
    ( '' ),
    'SwSTEP 2.0',
    'SolidWorks 2021',
    '' );
FILE_SCHEMA (( 'AUTOMOTIVE_DESIGN' ));
ENDSEC;

DATA;
#45=( NAMED_UNIT ( * ) PLANE_ANGLE_UNIT ( ) SI_UNIT ( $, .RADIAN. ) );
#66=FILL_AREA_STYLE ('',( #23440 ) ) ;
#105=AXIS2_PLACEMENT_3D ( 'NONE', #8951, #27958, #28266 ) ;
#360=( NAMED_UNIT ( * ) SI_UNIT ( $, .STERADIAN. ) SOLID_ANGLE_UNIT ( ) );
#371=VERTEX_POINT ( 'NONE', #11866 ) ;
#389=FILL_AREA_STYLE_COLOUR ( '', #23703 ) ;
#392=STYLED_ITEM ( 'NONE', ( #29024 ), #17172 ) ;
#491=( NAMED_UNIT ( * ) SI_UNIT ( $, .STERADIAN. ) SOLID_ANGLE_UNIT ( ) );
#541=FILL_AREA_STYLE ('',( #389 ) ) ;
#581=DIRECTION ( 'NONE',  ( 0.000000000000000000, -5.551115123125768527E-17, 1.000000000000000000 ) ) ;
#758=CIRCLE ( 'NONE', #17959, 6.500000000000016875 ) ;
#1106=DIRECTION ( 'NONE',  ( 0.000000000000000000, 5.551115123125767911E-17, -1.000000000000000000 ) ) ;
#1140=CLOSED_SHELL ( 'NONE', ( #15568, #6778, #2625, #29898, #6539, #6984, #26291, #17172, #11505, #2991 ) ) ;
#1141=EDGE_CURVE ( 'NONE', #17687, #30043, #25055, .T. ) ;
#1204=DIRECTION ( 'NONE',  ( 1.000000000000000000, 0.000000000000000000, 0.000000000000000000 ) ) ;
#1248=DIRECTION ( 'NONE',  ( -1.000000000000000000, 0.000000000000000000, 0.000000000000000000 ) ) ;
#1303=AXIS2_PLACEMENT_3D ( 'NONE', #27495, #22921, #6627 ) ;
#1557=COLOUR_RGB ( '', 0.66274510, 0.83137255, 0.94901961) ;
#1559=FILL_AREA_STYLE ('',( #25345 ) ) ;
#1604=PRODUCT_CONTEXT ( 'NONE', #13648, 'mechanical' ) ;
#1864=( NAMED_UNIT ( * ) SI_UNIT ( $, .STERADIAN. ) SOLID_ANGLE_UNIT ( ) );
#1889=EDGE_CURVE ( 'NONE', #14191, #4494, #24102, .T. ) ;
#1923=PRESENTATION_STYLE_ASSIGNMENT (( #23590 ) ) ;
#2049=CARTESIAN_POINT ( 'NONE',  ( 0.000000000000000000, 3.114577045054885743E-15, -17.50000000000004619 ) ) ;
#2069=CARTESIAN_POINT ( 'NONE',  ( 19.99999999999998934, 1.156842902448957494E-15, -6.500000000000016875 ) ) ;
#2180=AXIS2_PLACEMENT_3D ( 'NONE', #19791, #28990, #22824 ) ;
#2617=ORIENTED_EDGE ( 'NONE', *, *, #1141, .F. ) ;
#2625=ADVANCED_FACE ( 'NONE', ( #10439 ), #13499, .T. ) ;
#2873=UNCERTAINTY_MEASURE_WITH_UNIT (LENGTH_MEASURE( 1.000000000000000082E-05 ), #8792, 'distance_accuracy_value', 'NONE');
#2991=ADVANCED_FACE ( 'NONE', ( #17635 ), #27716, .T. ) ;
#3017=ADVANCED_BREP_SHAPE_REPRESENTATION ( '', ( #24254, #18805 ), #12447 ) ;
#3156=COLOUR_RGB ( '', 0.08235294, 0.09019608, 0.10196078) ;
#3172=FACE_OUTER_BOUND ( 'NONE', #24288, .T. ) ;
#3212=FILL_AREA_STYLE ('',( #24262 ) ) ;
#3222=VERTEX_POINT ( 'NONE', #10332 ) ;
#3294=DIRECTION ( 'NONE',  ( 0.000000000000000000, 5.551115123125767911E-17, -1.000000000000000000 ) ) ;
#3390=VECTOR ( 'NONE', #30280, 1000.000000000000114 ) ;
#3428=DIRECTION ( 'NONE',  ( 0.000000000000000000, 5.551115123125767911E-17, -1.000000000000000000 ) ) ;
#3502=EDGE_CURVE ( 'NONE', #27301, #22988, #24130, .T. ) ;
#3535=FACE_OUTER_BOUND ( 'NONE', #5228, .T. ) ;
#3595=DIRECTION ( 'NONE',  ( -1.000000000000000000, 0.000000000000000000, 0.000000000000000000 ) ) ;
#3604=DIRECTION ( 'NONE',  ( 0.000000000000000000, -5.551115123125768527E-17, 1.000000000000000000 ) ) ;
#3662=FACE_OUTER_BOUND ( 'NONE', #5787, .T. ) ;
#3671=SURFACE_STYLE_USAGE ( .BOTH. , #26860 ) ;
#3768=DIRECTION ( 'NONE',  ( 0.000000000000000000, 5.551115123125768527E-17, -1.000000000000000000 ) ) ;
#3849=DIRECTION ( 'NONE',  ( -1.000000000000000000, 0.000000000000000000, 0.000000000000000000 ) ) ;
#3989=ORIENTED_EDGE ( 'NONE', *, *, #21467, .T. ) ;
#4014=DIRECTION ( 'NONE',  ( 0.000000000000000000, -5.551115123125767911E-17, 1.000000000000000000 ) ) ;
#4114=ORIENTED_EDGE ( 'NONE', *, *, #17047, .F. ) ;
#4217=DIRECTION ( 'NONE',  ( 1.000000000000000000, 0.000000000000000000, 0.000000000000000000 ) ) ;
#4220=( NAMED_UNIT ( * ) PLANE_ANGLE_UNIT ( ) SI_UNIT ( $, .RADIAN. ) );
#4235=ORIENTED_EDGE ( 'NONE', *, *, #5864, .T. ) ;
#4321=PRESENTATION_STYLE_ASSIGNMENT (( #30123 ) ) ;
#4382=ORIENTED_EDGE ( 'NONE', *, *, #27363, .F. ) ;
#4407=ORIENTED_EDGE ( 'NONE', *, *, #30077, .T. ) ;
#4494=VERTEX_POINT ( 'NONE', #8032 ) ;
#4640=EDGE_LOOP ( 'NONE', ( #7307, #6228, #8668, #15125 ) ) ;
#4803=( LENGTH_UNIT ( ) NAMED_UNIT ( * ) SI_UNIT ( .MILLI., .METRE. ) );
#5019=UNCERTAINTY_MEASURE_WITH_UNIT (LENGTH_MEASURE( 1.000000000000000082E-05 ), #28319, 'distance_accuracy_value', 'NONE');
#5134=AXIS2_PLACEMENT_3D ( 'NONE', #25665, #30118, #18476 ) ;
#5227=AXIS2_PLACEMENT_3D ( 'NONE', #7110, #9887, #19261 ) ;
#5228=EDGE_LOOP ( 'NONE', ( #18941, #4407, #23790, #4382 ) ) ;
#5315=ORIENTED_EDGE ( 'NONE', *, *, #26063, .T. ) ;
#5501=( GEOMETRIC_REPRESENTATION_CONTEXT ( 3 ) GLOBAL_UNCERTAINTY_ASSIGNED_CONTEXT ( ( #16829 ) ) GLOBAL_UNIT_ASSIGNED_CONTEXT ( ( #13979, #19019, #25602 ) ) REPRESENTATION_CONTEXT ( 'NONE', 'WORKASPACE' ) );
#5527=CARTESIAN_POINT ( 'NONE',  ( 6.055081547227420202, 6.938893903907228378E-16, -12.50000000000003375 ) ) ;
#5553=CARTESIAN_POINT ( 'NONE',  ( 19.99999999999998934, -3.608224830031758756E-16, 6.500000000000016875 ) ) ;
#5616=VERTEX_POINT ( 'NONE', #13336 ) ;
#5666=CARTESIAN_POINT ( 'NONE',  ( 0.000000000000000000, 2.678141147339105664E-16, 4.000000000000000000 ) ) ;
#5675=FACE_OUTER_BOUND ( 'NONE', #9471, .T. ) ;
#5717=VECTOR ( 'NONE', #8671, 1000.000000000000114 ) ;
#5787=EDGE_LOOP ( 'NONE', ( #26251, #8710, #19864, #4114 ) ) ;
#5820=( NAMED_UNIT ( * ) SI_UNIT ( $, .STERADIAN. ) SOLID_ANGLE_UNIT ( ) );
#5846=DIRECTION ( 'NONE',  ( 0.000000000000000000, -5.551115123125767911E-17, 1.000000000000000000 ) ) ;
#5864=EDGE_CURVE ( 'NONE', #21338, #30043, #6962, .T. ) ;
#5909=CARTESIAN_POINT ( 'NONE',  ( 19.99999999999998934, 0.000000000000000000, 0.000000000000000000 ) ) ;
#5992=ORIENTED_EDGE ( 'NONE', *, *, #1889, .F. ) ;
#6228=ORIENTED_EDGE ( 'NONE', *, *, #14952, .T. ) ;
#6282=CARTESIAN_POINT ( 'NONE',  ( 6.055081547227420202, 0.000000000000000000, 0.000000000000000000 ) ) ;
#6351=CARTESIAN_POINT ( 'NONE',  ( 9.433704689814137012, 0.000000000000000000, 0.000000000000000000 ) ) ;
#6360=DIRECTION ( 'NONE',  ( 0.000000000000000000, -5.551115123125767911E-17, 1.000000000000000000 ) ) ;
#6482=CARTESIAN_POINT ( 'NONE',  ( 0.000000000000000000, 0.000000000000000000, 0.000000000000000000 ) ) ;
#6539=ADVANCED_FACE ( 'NONE', ( #7554, #7273 ), #12362, .F. ) ;
#6627=DIRECTION ( 'NONE',  ( 0.000000000000000000, 5.551115123125767911E-17, -1.000000000000000000 ) ) ;
#6633=CIRCLE ( 'NONE', #8074, 17.50000000000004619 ) ;
#6778=ADVANCED_FACE ( 'NONE', ( #25047 ), #16047, .F. ) ;
#6879=DIRECTION ( 'NONE',  ( 0.000000000000000000, 5.551115123125767911E-17, -1.000000000000000000 ) ) ;
#6956=MECHANICAL_DESIGN_GEOMETRIC_PRESENTATION_REPRESENTATION('',(#28035),#24121);
#6962=LINE ( 'NONE', #2069, #5717 ) ;
#6978=PRODUCT ( 'Rod base', 'Rod base', '', ( #1604 ) ) ;
#6980=( NAMED_UNIT ( * ) PLANE_ANGLE_UNIT ( ) SI_UNIT ( $, .RADIAN. ) );
#6984=ADVANCED_FACE ( 'NONE', ( #3535 ), #12966, .T. ) ;
#7110=CARTESIAN_POINT ( 'NONE',  ( 0.000000000000000000, 0.000000000000000000, 0.000000000000000000 ) ) ;
#7129=DIRECTION ( 'NONE',  ( 0.000000000000000000, -5.551115123125767911E-17, 1.000000000000000000 ) ) ;
#7162=( LENGTH_UNIT ( ) NAMED_UNIT ( * ) SI_UNIT ( .MILLI., .METRE. ) );
#7189=SHAPE_REPRESENTATION ( 'Rod base', ( #18805 ), #12447 ) ;
#7273=FACE_OUTER_BOUND ( 'NONE', #13050, .T. ) ;
#7307=ORIENTED_EDGE ( 'NONE', *, *, #9780, .F. ) ;
#7554=FACE_BOUND ( 'NONE', #7591, .T. ) ;
#7591=EDGE_LOOP ( 'NONE', ( #20472, #15837 ) ) ;
#7836=DIRECTION ( 'NONE',  ( 0.000000000000000000, 5.551115123125769144E-17, -1.000000000000000000 ) ) ;
#7990=DIRECTION ( 'NONE',  ( 0.000000000000000000, -1.000000000000000000, -5.551115123125767911E-17 ) ) ;
#8032=CARTESIAN_POINT ( 'NONE',  ( 0.000000000000000000, -9.714451465470119729E-16, 17.50000000000004619 ) ) ;
#8046=EDGE_CURVE ( 'NONE', #371, #3222, #18426, .T. ) ;
#8074=AXIS2_PLACEMENT_3D ( 'NONE', #24648, #3595, #6360 ) ;
#8201=UNCERTAINTY_MEASURE_WITH_UNIT (LENGTH_MEASURE( 1.000000000000000082E-05 ), #28461, 'distance_accuracy_value', 'NONE');
#8272=EDGE_LOOP ( 'NONE', ( #12136, #4235, #20762, #8930 ) ) ;
#8517=EDGE_CURVE ( 'NONE', #14191, #5616, #22860, .T. ) ;
#8568=STYLED_ITEM ( 'NONE', ( #17698 ), #24254 ) ;
#8668=ORIENTED_EDGE ( 'NONE', *, *, #8046, .T. ) ;
#8671=DIRECTION ( 'NONE',  ( -0.7371541402007405486, 1.202626523861922663E-16, -0.6757246285173472700 ) ) ;
#8710=ORIENTED_EDGE ( 'NONE', *, *, #9438, .T. ) ;
#8792=( LENGTH_UNIT ( ) NAMED_UNIT ( * ) SI_UNIT ( .MILLI., .METRE. ) );
#8930=ORIENTED_EDGE ( 'NONE', *, *, #26063, .F. ) ;
#8951=CARTESIAN_POINT ( 'NONE',  ( 6.055081547227420202, 0.000000000000000000, 0.000000000000000000 ) ) ;
#9188=EDGE_LOOP ( 'NONE', ( #22454, #19334 ) ) ;
#9284=DIRECTION ( 'NONE',  ( 0.000000000000000000, 1.000000000000000000, -6.695352868347764161E-17 ) ) ;
#9324=SHAPE_REPRESENTATION_RELATIONSHIP ( 'NONE' , 'NONE' ,  #7189, #3017 ) ;
#9438=EDGE_CURVE ( 'NONE', #14191, #17687, #17293, .T. ) ;
#9452=CARTESIAN_POINT ( 'NONE',  ( 19.99999999999998934, 6.500000000000061284, 4.163336342344337027E-14 ) ) ;
#9471=EDGE_LOOP ( 'NONE', ( #27486, #27717 ) ) ;
#9497=APPLICATION_CONTEXT ( 'automotive_design' ) ;
#9627=PRESENTATION_STYLE_ASSIGNMENT (( #14133 ) ) ;
#9665=COLOUR_RGB ( '', 0.72549020, 0.75294118, 0.79215686) ;
#9691=DIRECTION ( 'NONE',  ( 1.000000000000000000, 0.000000000000000000, 0.000000000000000000 ) ) ;
#9780=EDGE_CURVE ( 'NONE', #22988, #27301, #15324, .T. ) ;
#9887=DIRECTION ( 'NONE',  ( 1.000000000000000000, 0.000000000000000000, 0.000000000000000000 ) ) ;
#9994=ORIENTED_EDGE ( 'NONE', *, *, #8517, .T. ) ;
#10065=CARTESIAN_POINT ( 'NONE',  ( 19.99999999999998934, 2.018759447849275454E-15, -6.500000000000000000 ) ) ;
#10089=VECTOR ( 'NONE', #22944, 1000.000000000000000 ) ;
#10118=ORIENTED_EDGE ( 'NONE', *, *, #12141, .T. ) ;
#10162=( NAMED_UNIT ( * ) PLANE_ANGLE_UNIT ( ) SI_UNIT ( $, .RADIAN. ) );
#10293=VECTOR ( 'NONE', #4217, 1000.000000000000000 ) ;
#10318=SURFACE_STYLE_USAGE ( .BOTH. , #12089 ) ;
#10330=DIRECTION ( 'NONE',  ( -1.000000000000000000, 0.000000000000000000, 0.000000000000000000 ) ) ;
#10332=CARTESIAN_POINT ( 'NONE',  ( 19.99999999999998934, 2.220446049250313081E-16, -4.000000000000010658 ) ) ;
#10350=CARTESIAN_POINT ( 'NONE',  ( 0.000000000000000000, 0.000000000000000000, 0.000000000000000000 ) ) ;
#10439=FACE_OUTER_BOUND ( 'NONE', #8272, .T. ) ;
#10657=CYLINDRICAL_SURFACE ( 'NONE', #17298, 17.50000000000004619 ) ;
#10659=COLOUR_RGB ( '', 0.09019608, 0.27058824, 0.51372549) ;
#11038=DIRECTION ( 'NONE',  ( 0.000000000000000000, 0.000000000000000000, 1.000000000000000000 ) ) ;
#11078=DIRECTION ( 'NONE',  ( 0.000000000000000000, 5.551115123125768527E-17, -1.000000000000000000 ) ) ;
#11317=CARTESIAN_POINT ( 'NONE',  ( 6.055081547227420202, 8.369191085434727264E-16, 12.50000000000003375 ) ) ;
#11376=CIRCLE ( 'NONE', #25560, 4.000000000000010658 ) ;
#11489=DIRECTION ( 'NONE',  ( 0.000000000000000000, 5.551115123125767911E-17, -1.000000000000000000 ) ) ;
#11505=ADVANCED_FACE ( 'NONE', ( #14252 ), #21281, .F. ) ;
#11636=CARTESIAN_POINT ( 'NONE',  ( -27.00000000000002487, 2.220446049250313081E-16, -4.000000000000010658 ) ) ;
#11641=CARTESIAN_POINT ( 'NONE',  ( 9.433704689814137012, 0.000000000000000000, 0.000000000000000000 ) ) ;
#11688=CARTESIAN_POINT ( 'NONE',  ( 19.99999999999998934, 0.000000000000000000, 0.000000000000000000 ) ) ;
#11866=CARTESIAN_POINT ( 'NONE',  ( 19.99999999999998934, 2.678141147339105664E-16, 4.000000000000000000 ) ) ;
#12089=SURFACE_SIDE_STYLE ('',( #14103 ) ) ;
#12136=ORIENTED_EDGE ( 'NONE', *, *, #21116, .T. ) ;
#12141=EDGE_CURVE ( 'NONE', #3222, #371, #11376, .T. ) ;
#12224=FILL_AREA_STYLE ('',( #24001 ) ) ;
#12229=UNCERTAINTY_MEASURE_WITH_UNIT (LENGTH_MEASURE( 1.000000000000000082E-05 ), #7162, 'distance_accuracy_value', 'NONE');
#12253=UNCERTAINTY_MEASURE_WITH_UNIT (LENGTH_MEASURE( 1.000000000000000082E-05 ), #4803, 'distance_accuracy_value', 'NONE');
#12265=( NAMED_UNIT ( * ) SI_UNIT ( $, .STERADIAN. ) SOLID_ANGLE_UNIT ( ) );
#12334=EDGE_CURVE ( 'NONE', #21338, #13036, #29477, .T. ) ;
#12362=PLANE ( 'NONE',  #5227 ) ;
#12406=ORIENTED_EDGE ( 'NONE', *, *, #12334, .T. ) ;
#12447=( GEOMETRIC_REPRESENTATION_CONTEXT ( 3 ) GLOBAL_UNCERTAINTY_ASSIGNED_CONTEXT ( ( #12229 ) ) GLOBAL_UNIT_ASSIGNED_CONTEXT ( ( #7162, #21608, #12265 ) ) REPRESENTATION_CONTEXT ( 'NONE', 'WORKASPACE' ) );
#12966=CYLINDRICAL_SURFACE ( 'NONE', #16581, 17.50000000000004619 ) ;
#13036=VERTEX_POINT ( 'NONE', #5553 ) ;
#13050=EDGE_LOOP ( 'NONE', ( #14618, #25457 ) ) ;
#13336=CARTESIAN_POINT ( 'NONE',  ( 6.055081547227420202, 3.114577045054877854E-15, -17.50000000000000000 ) ) ;
#13416=MECHANICAL_DESIGN_GEOMETRIC_PRESENTATION_REPRESENTATION('',(#15387),#5501);
#13499=CONICAL_SURFACE ( 'NONE', #2180, 6.500000000000016875, 0.7419472680059175929 ) ;
#13533=CARTESIAN_POINT ( 'NONE',  ( 6.055081547227420202, 0.000000000000000000, 0.000000000000000000 ) ) ;
#13581=SURFACE_STYLE_FILL_AREA ( #1559 ) ;
#13648=APPLICATION_CONTEXT ( 'automotive_design' ) ;
#13688=CIRCLE ( 'NONE', #15136, 4.999999999999999112 ) ;
#13812=CIRCLE ( 'NONE', #29445, 17.50000000000004619 ) ;
#13979=( LENGTH_UNIT ( ) NAMED_UNIT ( * ) SI_UNIT ( .MILLI., .METRE. ) );
#14019=MECHANICAL_DESIGN_GEOMETRIC_PRESENTATION_REPRESENTATION('',(#8568),#16934);
#14085=SURFACE_SIDE_STYLE ('',( #23858 ) ) ;
#14103=SURFACE_STYLE_FILL_AREA ( #66 ) ;
#14133=SURFACE_STYLE_USAGE ( .BOTH. , #16576 ) ;
#14191=VERTEX_POINT ( 'NONE', #18498 ) ;
#14252=FACE_OUTER_BOUND ( 'NONE', #14543, .T. ) ;
#14483=ORIENTED_EDGE ( 'NONE', *, *, #17047, .T. ) ;
#14543=EDGE_LOOP ( 'NONE', ( #20912, #23921, #30406, #10118 ) ) ;
#14618=ORIENTED_EDGE ( 'NONE', *, *, #16877, .T. ) ;
#14631=LINE ( 'NONE', #16499, #3390 ) ;
#14710=DIRECTION ( 'NONE',  ( 1.000000000000000000, 0.000000000000000000, 0.000000000000000000 ) ) ;
#14952=EDGE_CURVE ( 'NONE', #22988, #371, #28164, .T. ) ;
#15125=ORIENTED_EDGE ( 'NONE', *, *, #16980, .F. ) ;
#15136=AXIS2_PLACEMENT_3D ( 'NONE', #5527, #7990, #7836 ) ;
#15207=EDGE_LOOP ( 'NONE', ( #9994, #3989, #19490, #5992 ) ) ;
#15211=CONICAL_SURFACE ( 'NONE', #23562, 6.500000000000016875, 0.7419472680059175929 ) ;
#15324=CIRCLE ( 'NONE', #23162, 4.000000000000010658 ) ;
#15343=CARTESIAN_POINT ( 'NONE',  ( 6.055081547227420202, 0.000000000000000000, 0.000000000000000000 ) ) ;
#15387=STYLED_ITEM ( 'NONE', ( #9627 ), #3017 ) ;
#15416=PRODUCT_DEFINITION_FORMATION_WITH_SPECIFIED_SOURCE ( 'ANY', '', #6978, .NOT_KNOWN. ) ;
#15568=ADVANCED_FACE ( 'NONE', ( #3662 ), #17168, .T. ) ;
#15642=MECHANICAL_DESIGN_GEOMETRIC_PRESENTATION_REPRESENTATION('',(#392),#22474);
#15837=ORIENTED_EDGE ( 'NONE', *, *, #9780, .T. ) ;
#16047=CYLINDRICAL_SURFACE ( 'NONE', #1303, 4.000000000000010658 ) ;
#16106=FILL_AREA_STYLE ('',( #25729 ) ) ;
#16282=SURFACE_STYLE_FILL_AREA ( #541 ) ;
#16390=DIRECTION ( 'NONE',  ( 0.000000000000000000, 6.695352868347765393E-17, 1.000000000000000000 ) ) ;
#16397=FACE_BOUND ( 'NONE', #9188, .T. ) ;
#16499=CARTESIAN_POINT ( 'NONE',  ( 19.99999999999998934, -3.608224830031758756E-16, 6.500000000000016875 ) ) ;
#16576=SURFACE_SIDE_STYLE ('',( #16282 ) ) ;
#16581=AXIS2_PLACEMENT_3D ( 'NONE', #17562, #10330, #24282 ) ;
#16824=SURFACE_STYLE_USAGE ( .BOTH. , #14085 ) ;
#16829=UNCERTAINTY_MEASURE_WITH_UNIT (LENGTH_MEASURE( 1.000000000000000082E-05 ), #13979, 'distance_accuracy_value', 'NONE');
#16877=EDGE_CURVE ( 'NONE', #4494, #29584, #6633, .T. ) ;
#16923=CARTESIAN_POINT ( 'NONE',  ( 0.000000000000000000, -9.714451465470119729E-16, 17.50000000000004619 ) ) ;
#16934=( GEOMETRIC_REPRESENTATION_CONTEXT ( 3 ) GLOBAL_UNCERTAINTY_ASSIGNED_CONTEXT ( ( #21318 ) ) GLOBAL_UNIT_ASSIGNED_CONTEXT ( ( #22286, #10162, #5820 ) ) REPRESENTATION_CONTEXT ( 'NONE', 'WORKASPACE' ) );
#16969=PRESENTATION_STYLE_ASSIGNMENT (( #16824 ) ) ;
#16980=EDGE_CURVE ( 'NONE', #27301, #3222, #20508, .T. ) ;
#17047=EDGE_CURVE ( 'NONE', #5616, #30043, #13688, .T. ) ;
#17168=TOROIDAL_SURFACE ( 'NONE', #27425, 12.50000000000000000, 5.000000000000000000 ) ;
#17172=ADVANCED_FACE ( 'NONE', ( #16397, #5675 ), #28315, .F. ) ;
#17243=SURFACE_STYLE_FILL_AREA ( #3212 ) ;
#17281=DIRECTION ( 'NONE',  ( 1.000000000000000000, 0.000000000000000000, 0.000000000000000000 ) ) ;
#17293=CIRCLE ( 'NONE', #20216, 4.999999999999999112 ) ;
#17298=AXIS2_PLACEMENT_3D ( 'NONE', #6482, #1248, #4014 ) ;
#17309=AXIS2_PLACEMENT_3D ( 'NONE', #23142, #20832, #18538 ) ;
#17562=CARTESIAN_POINT ( 'NONE',  ( 0.000000000000000000, 0.000000000000000000, 0.000000000000000000 ) ) ;
#17635=FACE_OUTER_BOUND ( 'NONE', #28916, .T. ) ;
#17687=VERTEX_POINT ( 'NONE', #27110 ) ;
#17698=PRESENTATION_STYLE_ASSIGNMENT (( #3671 ) ) ;
#17959=AXIS2_PLACEMENT_3D ( 'NONE', #5909, #29577, #3604 ) ;
#18034=( NAMED_UNIT ( * ) PLANE_ANGLE_UNIT ( ) SI_UNIT ( $, .RADIAN. ) );
#18259=DIRECTION ( 'NONE',  ( 1.000000000000000000, 0.000000000000000000, 0.000000000000000000 ) ) ;
#18426=CIRCLE ( 'NONE', #5134, 4.000000000000010658 ) ;
#18476=DIRECTION ( 'NONE',  ( 0.000000000000000000, 5.551115123125767911E-17, -1.000000000000000000 ) ) ;
#18482=SURFACE_SIDE_STYLE ('',( #13581 ) ) ;
#18498=CARTESIAN_POINT ( 'NONE',  ( 6.055081547227420202, -9.714451465470096063E-16, 17.50000000000000000 ) ) ;
#18515=( GEOMETRIC_REPRESENTATION_CONTEXT ( 3 ) GLOBAL_UNCERTAINTY_ASSIGNED_CONTEXT ( ( #12253 ) ) GLOBAL_UNIT_ASSIGNED_CONTEXT ( ( #4803, #45, #491 ) ) REPRESENTATION_CONTEXT ( 'NONE', 'WORKASPACE' ) );
#18538=DIRECTION ( 'NONE',  ( 0.000000000000000000, 5.551115123125767911E-17, -1.000000000000000000 ) ) ;
#18805=AXIS2_PLACEMENT_3D ( 'NONE', #20700, #11038, #18259 ) ;
#18833=DIRECTION ( 'NONE',  ( -1.000000000000000000, 0.000000000000000000, 0.000000000000000000 ) ) ;
#18941=ORIENTED_EDGE ( 'NONE', *, *, #21467, .F. ) ;
#18996=SURFACE_STYLE_FILL_AREA ( #16106 ) ;
#19000=LINE ( 'NONE', #2049, #10089 ) ;
#19019=( NAMED_UNIT ( * ) PLANE_ANGLE_UNIT ( ) SI_UNIT ( $, .RADIAN. ) );
#19242=AXIS2_PLACEMENT_3D ( 'NONE', #24199, #14710, #3294 ) ;
#19261=DIRECTION ( 'NONE',  ( 0.000000000000000000, 5.551115123125767911E-17, -1.000000000000000000 ) ) ;
#19334=ORIENTED_EDGE ( 'NONE', *, *, #8046, .F. ) ;
#19396=AXIS2_PLACEMENT_3D ( 'NONE', #11641, #30027, #11489 ) ;
#19490=ORIENTED_EDGE ( 'NONE', *, *, #16877, .F. ) ;
#19681=AXIS2_PLACEMENT_3D ( 'NONE', #6351, #24480, #3428 ) ;
#19772=CARTESIAN_POINT ( 'NONE',  ( 19.99999999999998934, 0.000000000000000000, 0.000000000000000000 ) ) ;
#19791=CARTESIAN_POINT ( 'NONE',  ( 19.99999999999998934, 0.000000000000000000, 0.000000000000000000 ) ) ;
#19864=ORIENTED_EDGE ( 'NONE', *, *, #20313, .F. ) ;
#20216=AXIS2_PLACEMENT_3D ( 'NONE', #11317, #9284, #16390 ) ;
#20311=ORIENTED_EDGE ( 'NONE', *, *, #30077, .F. ) ;
#20313=EDGE_CURVE ( 'NONE', #30043, #17687, #20878, .T. ) ;
#20472=ORIENTED_EDGE ( 'NONE', *, *, #3502, .T. ) ;
#20503=SHAPE_DEFINITION_REPRESENTATION ( #28061, #7189 ) ;
#20508=LINE ( 'NONE', #11636, #29170 ) ;
#20700=CARTESIAN_POINT ( 'NONE',  ( 0.000000000000000000, 0.000000000000000000, 0.000000000000000000 ) ) ;
#20757=ORIENTED_EDGE ( 'NONE', *, *, #9438, .F. ) ;
#20762=ORIENTED_EDGE ( 'NONE', *, *, #20313, .T. ) ;
#20832=DIRECTION ( 'NONE',  ( 1.000000000000000000, 0.000000000000000000, 0.000000000000000000 ) ) ;
#20878=CIRCLE ( 'NONE', #19396, 16.18577070100374726 ) ;
#20888=AXIS2_PLACEMENT_3D ( 'NONE', #15343, #24821, #3768 ) ;
#20912=ORIENTED_EDGE ( 'NONE', *, *, #14952, .F. ) ;
#20982=DIRECTION ( 'NONE',  ( 1.000000000000000000, 0.000000000000000000, 0.000000000000000000 ) ) ;
#21116=EDGE_CURVE ( 'NONE', #13036, #21338, #758, .T. ) ;
#21281=CYLINDRICAL_SURFACE ( 'NONE', #17309, 4.000000000000010658 ) ;
#21318=UNCERTAINTY_MEASURE_WITH_UNIT (LENGTH_MEASURE( 1.000000000000000082E-05 ), #22286, 'distance_accuracy_value', 'NONE');
#21338=VERTEX_POINT ( 'NONE', #10065 ) ;
#21399=AXIS2_PLACEMENT_3D ( 'NONE', #13533, #27752, #6879 ) ;
#21467=EDGE_CURVE ( 'NONE', #5616, #29584, #19000, .T. ) ;
#21521=DIRECTION ( 'NONE',  ( 0.000000000000000000, 5.551115123125767911E-17, -1.000000000000000000 ) ) ;
#21608=( NAMED_UNIT ( * ) PLANE_ANGLE_UNIT ( ) SI_UNIT ( $, .RADIAN. ) );
#21936=DIRECTION ( 'NONE',  ( -1.000000000000000000, 0.000000000000000000, 0.000000000000000000 ) ) ;
#22286=( LENGTH_UNIT ( ) NAMED_UNIT ( * ) SI_UNIT ( .MILLI., .METRE. ) );
#22454=ORIENTED_EDGE ( 'NONE', *, *, #12141, .F. ) ;
#22474=( GEOMETRIC_REPRESENTATION_CONTEXT ( 3 ) GLOBAL_UNCERTAINTY_ASSIGNED_CONTEXT ( ( #8201 ) ) GLOBAL_UNIT_ASSIGNED_CONTEXT ( ( #28461, #6980, #360 ) ) REPRESENTATION_CONTEXT ( 'NONE', 'WORKASPACE' ) );
#22824=DIRECTION ( 'NONE',  ( 0.000000000000000000, -5.551115123125768527E-17, 1.000000000000000000 ) ) ;
#22860=CIRCLE ( 'NONE', #21399, 17.50000000000004619 ) ;
#22921=DIRECTION ( 'NONE',  ( 1.000000000000000000, 0.000000000000000000, 0.000000000000000000 ) ) ;
#22944=DIRECTION ( 'NONE',  ( -1.000000000000000000, 0.000000000000000000, 0.000000000000000000 ) ) ;
#22988=VERTEX_POINT ( 'NONE', #5666 ) ;
#23142=CARTESIAN_POINT ( 'NONE',  ( -27.00000000000002487, 0.000000000000000000, 0.000000000000000000 ) ) ;
#23162=AXIS2_PLACEMENT_3D ( 'NONE', #10350, #17281, #1106 ) ;
#23297=( NAMED_UNIT ( * ) SI_UNIT ( $, .STERADIAN. ) SOLID_ANGLE_UNIT ( ) );
#23440=FILL_AREA_STYLE_COLOUR ( '', #29330 ) ;
#23474=AXIS2_PLACEMENT_3D ( 'NONE', #9452, #18833, #7129 ) ;
#23562=AXIS2_PLACEMENT_3D ( 'NONE', #19772, #21936, #581 ) ;
#23590=SURFACE_STYLE_USAGE ( .BOTH. , #25409 ) ;
#23703=COLOUR_RGB ( '', 0.08235294, 0.09019608, 0.10196078) ;
#23790=ORIENTED_EDGE ( 'NONE', *, *, #1889, .T. ) ;
#23858=SURFACE_STYLE_FILL_AREA ( #12224 ) ;
#23863=PRODUCT_DEFINITION_CONTEXT ( 'detailed design', #9497, 'design' ) ;
#23921=ORIENTED_EDGE ( 'NONE', *, *, #3502, .F. ) ;
#24001=FILL_AREA_STYLE_COLOUR ( '', #10659 ) ;
#24102=LINE ( 'NONE', #16923, #29764 ) ;
#24121=( GEOMETRIC_REPRESENTATION_CONTEXT ( 3 ) GLOBAL_UNCERTAINTY_ASSIGNED_CONTEXT ( ( #5019 ) ) GLOBAL_UNIT_ASSIGNED_CONTEXT ( ( #28319, #4220, #23297 ) ) REPRESENTATION_CONTEXT ( 'NONE', 'WORKASPACE' ) );
#24130=CIRCLE ( 'NONE', #19242, 4.000000000000010658 ) ;
#24199=CARTESIAN_POINT ( 'NONE',  ( 0.000000000000000000, 0.000000000000000000, 0.000000000000000000 ) ) ;
#24254=MANIFOLD_SOLID_BREP ( 'Fillet1', #1140 ) ;
#24262=FILL_AREA_STYLE_COLOUR ( '', #3156 ) ;
#24282=DIRECTION ( 'NONE',  ( 0.000000000000000000, -5.551115123125767911E-17, 1.000000000000000000 ) ) ;
#24288=EDGE_LOOP ( 'NONE', ( #28487, #12406, #5315, #30269 ) ) ;
#24480=DIRECTION ( 'NONE',  ( 1.000000000000000000, 0.000000000000000000, 0.000000000000000000 ) ) ;
#24648=CARTESIAN_POINT ( 'NONE',  ( 0.000000000000000000, 0.000000000000000000, 0.000000000000000000 ) ) ;
#24821=DIRECTION ( 'NONE',  ( 1.000000000000000000, 0.000000000000000000, 0.000000000000000000 ) ) ;
#24902=CARTESIAN_POINT ( 'NONE',  ( 0.000000000000000000, 0.000000000000000000, 0.000000000000000000 ) ) ;
#25047=FACE_OUTER_BOUND ( 'NONE', #4640, .T. ) ;
#25055=CIRCLE ( 'NONE', #19681, 16.18577070100374726 ) ;
#25345=FILL_AREA_STYLE_COLOUR ( '', #9665 ) ;
#25409=SURFACE_SIDE_STYLE ('',( #18996 ) ) ;
#25457=ORIENTED_EDGE ( 'NONE', *, *, #27363, .T. ) ;
#25560=AXIS2_PLACEMENT_3D ( 'NONE', #26249, #9691, #21521 ) ;
#25570=CARTESIAN_POINT ( 'NONE',  ( -27.00000000000002487, 2.678141147339112567E-16, 4.000000000000010658 ) ) ;
#25602=( NAMED_UNIT ( * ) SI_UNIT ( $, .STERADIAN. ) SOLID_ANGLE_UNIT ( ) );
#25608=CIRCLE ( 'NONE', #105, 17.50000000000004619 ) ;
#25622=DIRECTION ( 'NONE',  ( -1.000000000000000000, 0.000000000000000000, 0.000000000000000000 ) ) ;
#25665=CARTESIAN_POINT ( 'NONE',  ( 19.99999999999998934, 0.000000000000000000, 0.000000000000000000 ) ) ;
#25729=FILL_AREA_STYLE_COLOUR ( '', #1557 ) ;
#25839=STYLED_ITEM ( 'NONE', ( #16969 ), #6539 ) ;
#26063=EDGE_CURVE ( 'NONE', #13036, #17687, #14631, .T. ) ;
#26249=CARTESIAN_POINT ( 'NONE',  ( 19.99999999999998934, 0.000000000000000000, 0.000000000000000000 ) ) ;
#26251=ORIENTED_EDGE ( 'NONE', *, *, #8517, .F. ) ;
#26291=ADVANCED_FACE ( 'NONE', ( #3172 ), #15211, .T. ) ;
#26558=CARTESIAN_POINT ( 'NONE',  ( 0.000000000000000000, 2.220446049250313081E-16, -4.000000000000010658 ) ) ;
#26860=SURFACE_SIDE_STYLE ('',( #17243 ) ) ;
#26891=FACE_OUTER_BOUND ( 'NONE', #15207, .T. ) ;
#26970=CARTESIAN_POINT ( 'NONE',  ( 0.000000000000000000, 3.114577045054877854E-15, -17.50000000000000000 ) ) ;
#27110=CARTESIAN_POINT ( 'NONE',  ( 9.433704689814137012, -8.984907651778784631E-16, 16.18577070100374371 ) ) ;
#27276=MECHANICAL_DESIGN_GEOMETRIC_PRESENTATION_REPRESENTATION('',(#27787),#28745);
#27301=VERTEX_POINT ( 'NONE', #26558 ) ;
#27363=EDGE_CURVE ( 'NONE', #29584, #4494, #13812, .T. ) ;
#27425=AXIS2_PLACEMENT_3D ( 'NONE', #6282, #1204, #11078 ) ;
#27486=ORIENTED_EDGE ( 'NONE', *, *, #21116, .F. ) ;
#27495=CARTESIAN_POINT ( 'NONE',  ( -27.00000000000002487, 0.000000000000000000, 0.000000000000000000 ) ) ;
#27716=TOROIDAL_SURFACE ( 'NONE', #20888, 12.50000000000000000, 5.000000000000000000 ) ;
#27717=ORIENTED_EDGE ( 'NONE', *, *, #12334, .F. ) ;
#27752=DIRECTION ( 'NONE',  ( -1.000000000000000000, -0.000000000000000000, -0.000000000000000000 ) ) ;
#27787=STYLED_ITEM ( 'NONE', ( #4321 ), #6778 ) ;
#27958=DIRECTION ( 'NONE',  ( -1.000000000000000000, -0.000000000000000000, -0.000000000000000000 ) ) ;
#28035=STYLED_ITEM ( 'NONE', ( #1923 ), #11505 ) ;
#28061=PRODUCT_DEFINITION_SHAPE ( 'NONE', 'NONE',  #29032 ) ;
#28117=CARTESIAN_POINT ( 'NONE',  ( 9.433704689814137012, 2.880675993249602881E-15, -16.18577070100374371 ) ) ;
#28164=LINE ( 'NONE', #25570, #10293 ) ;
#28266=DIRECTION ( 'NONE',  ( 0.000000000000000000, 5.551115123125767911E-17, -1.000000000000000000 ) ) ;
#28315=PLANE ( 'NONE',  #23474 ) ;
#28319=( LENGTH_UNIT ( ) NAMED_UNIT ( * ) SI_UNIT ( .MILLI., .METRE. ) );
#28461=( LENGTH_UNIT ( ) NAMED_UNIT ( * ) SI_UNIT ( .MILLI., .METRE. ) );
#28487=ORIENTED_EDGE ( 'NONE', *, *, #5864, .F. ) ;
#28488=AXIS2_PLACEMENT_3D ( 'NONE', #11688, #25622, #29757 ) ;
#28745=( GEOMETRIC_REPRESENTATION_CONTEXT ( 3 ) GLOBAL_UNCERTAINTY_ASSIGNED_CONTEXT ( ( #2873 ) ) GLOBAL_UNIT_ASSIGNED_CONTEXT ( ( #8792, #18034, #1864 ) ) REPRESENTATION_CONTEXT ( 'NONE', 'WORKASPACE' ) );
#28844=DIRECTION ( 'NONE',  ( -1.000000000000000000, 0.000000000000000000, 0.000000000000000000 ) ) ;
#28916=EDGE_LOOP ( 'NONE', ( #20757, #20311, #14483, #2617 ) ) ;
#28990=DIRECTION ( 'NONE',  ( -1.000000000000000000, 0.000000000000000000, 0.000000000000000000 ) ) ;
#29024=PRESENTATION_STYLE_ASSIGNMENT (( #10318 ) ) ;
#29032=PRODUCT_DEFINITION ( 'UNKNOWN', '', #15416, #23863 ) ;
#29170=VECTOR ( 'NONE', #20982, 1000.000000000000000 ) ;
#29246=MECHANICAL_DESIGN_GEOMETRIC_PRESENTATION_REPRESENTATION('',(#25839),#18515);
#29330=COLOUR_RGB ( '', 0.40784314, 0.44705882, 0.49803922) ;
#29445=AXIS2_PLACEMENT_3D ( 'NONE', #24902, #3849, #5846 ) ;
#29477=CIRCLE ( 'NONE', #28488, 6.500000000000016875 ) ;
#29577=DIRECTION ( 'NONE',  ( -1.000000000000000000, 0.000000000000000000, 0.000000000000000000 ) ) ;
#29584=VERTEX_POINT ( 'NONE', #26970 ) ;
#29757=DIRECTION ( 'NONE',  ( 0.000000000000000000, -5.551115123125768527E-17, 1.000000000000000000 ) ) ;
#29764=VECTOR ( 'NONE', #28844, 1000.000000000000000 ) ;
#29898=ADVANCED_FACE ( 'NONE', ( #26891 ), #10657, .T. ) ;
#30027=DIRECTION ( 'NONE',  ( 1.000000000000000000, 0.000000000000000000, 0.000000000000000000 ) ) ;
#30043=VERTEX_POINT ( 'NONE', #28117 ) ;
#30077=EDGE_CURVE ( 'NONE', #5616, #14191, #25608, .T. ) ;
#30118=DIRECTION ( 'NONE',  ( 1.000000000000000000, 0.000000000000000000, 0.000000000000000000 ) ) ;
#30123=SURFACE_STYLE_USAGE ( .BOTH. , #18482 ) ;
#30269=ORIENTED_EDGE ( 'NONE', *, *, #1141, .T. ) ;
#30280=DIRECTION ( 'NONE',  ( -0.7371541402007405486, -3.751025204431188723E-17, 0.6757246285173472700 ) ) ;
#30406=ORIENTED_EDGE ( 'NONE', *, *, #16980, .T. ) ;
ENDSEC;
END-ISO-10303-21;
